ISO-10303-21;
HEADER;
/* Generated by software containing ST-Developer
 * from STEP Tools, Inc. (www.steptools.com) 
 */

FILE_DESCRIPTION(
/* description */ ('Bell-crank linkage with push rods'),
/* implementation_level */ '2;1');

FILE_NAME(
/* name */ 'Upper pin sleeve (2).step',
/* time_stamp */ '2026-10-28T03:25:15-07:00',
/* author */ (''),
/* organization */ (''),
/* preprocessor_version */ 'ST-DEVELOPER v20.2',
/* originating_system */ 'Autodesk Translation Framework v15.17.0.0',
/* authorisation */ '');

FILE_SCHEMA (('AUTOMOTIVE_DESIGN { 1 0 10303 214 3 1 1 }'));
ENDSEC;

DATA;
#10=MECHANICAL_DESIGN_GEOMETRIC_PRESENTATION_REPRESENTATION('',(#654),#16678);
#538=SHAPE_REPRESENTATION_RELATIONSHIP('SRR','None',#16959,#592);
#592=ADVANCED_BREP_SHAPE_REPRESENTATION('',(#714),#16664);
#654=STYLED_ITEM('',(#17291),#714);
#714=MANIFOLD_SOLID_BREP('Body1',#8846);
#910=FACE_BOUND('',#2374,.T.);
#911=FACE_BOUND('',#2376,.T.);
#1185=PLANE('',#10339);
#1186=PLANE('',#10340);
#1664=FACE_OUTER_BOUND('',#2371,.T.);
#1665=FACE_OUTER_BOUND('',#2372,.T.);
#1666=FACE_OUTER_BOUND('',#2373,.T.);
#1667=FACE_OUTER_BOUND('',#2375,.T.);
#2371=EDGE_LOOP('',(#7659,#7660,#7661,#7662));
#2372=EDGE_LOOP('',(#7663,#7664,#7665,#7666));
#2373=EDGE_LOOP('',(#7667));
#2374=EDGE_LOOP('',(#7668));
#2375=EDGE_LOOP('',(#7669));
#2376=EDGE_LOOP('',(#7670));
#2966=LINE('',#16008,#3515);
#2967=LINE('',#16014,#3516);
#3515=VECTOR('',#12826,0.305);
#3516=VECTOR('',#12833,0.5);
#4031=CIRCLE('',#10334,0.305);
#4032=CIRCLE('',#10335,0.305);
#4033=CIRCLE('',#10337,0.5);
#4034=CIRCLE('',#10338,0.5);
#4698=VERTEX_POINT('',#16005);
#4699=VERTEX_POINT('',#16007);
#4700=VERTEX_POINT('',#16011);
#4701=VERTEX_POINT('',#16013);
#5707=EDGE_CURVE('',#4698,#4698,#4031,.T.);
#5708=EDGE_CURVE('',#4698,#4699,#2966,.T.);
#5709=EDGE_CURVE('',#4699,#4699,#4032,.T.);
#5710=EDGE_CURVE('',#4700,#4700,#4033,.T.);
#5711=EDGE_CURVE('',#4700,#4701,#2967,.T.);
#5712=EDGE_CURVE('',#4701,#4701,#4034,.T.);
#7659=ORIENTED_EDGE('',*,*,#5707,.F.);
#7660=ORIENTED_EDGE('',*,*,#5708,.T.);
#7661=ORIENTED_EDGE('',*,*,#5709,.T.);
#7662=ORIENTED_EDGE('',*,*,#5708,.F.);
#7663=ORIENTED_EDGE('',*,*,#5710,.F.);
#7664=ORIENTED_EDGE('',*,*,#5711,.T.);
#7665=ORIENTED_EDGE('',*,*,#5712,.T.);
#7666=ORIENTED_EDGE('',*,*,#5711,.F.);
#7667=ORIENTED_EDGE('',*,*,#5710,.T.);
#7668=ORIENTED_EDGE('',*,*,#5707,.T.);
#7669=ORIENTED_EDGE('',*,*,#5712,.F.);
#7670=ORIENTED_EDGE('',*,*,#5709,.F.);
#8232=CYLINDRICAL_SURFACE('',#10333,0.305);
#8233=CYLINDRICAL_SURFACE('',#10336,0.5);
#8689=ADVANCED_FACE('',(#1664),#8232,.F.);
#8690=ADVANCED_FACE('',(#1665),#8233,.T.);
#8691=ADVANCED_FACE('',(#1666,#910),#1185,.T.);
#8692=ADVANCED_FACE('',(#1667,#911),#1186,.F.);
#8846=CLOSED_SHELL('',(#8689,#8690,#8691,#8692));
#10332=AXIS2_PLACEMENT_3D('',#16003,#12820,#12821);
#10333=AXIS2_PLACEMENT_3D('',#16004,#12822,#12823);
#10334=AXIS2_PLACEMENT_3D('',#16006,#12824,#12825);
#10335=AXIS2_PLACEMENT_3D('',#16009,#12827,#12828);
#10336=AXIS2_PLACEMENT_3D('',#16010,#12829,#12830);
#10337=AXIS2_PLACEMENT_3D('',#16012,#12831,#12832);
#10338=AXIS2_PLACEMENT_3D('',#16015,#12834,#12835);
#10339=AXIS2_PLACEMENT_3D('',#16016,#12836,#12837);
#10340=AXIS2_PLACEMENT_3D('',#16017,#12838,#12839);
#12820=DIRECTION('axis',(0.,0.,1.));
#12821=DIRECTION('refdir',(1.,0.,0.));
#12822=DIRECTION('center_axis',(0.,0.,1.));
#12823=DIRECTION('ref_axis',(1.,0.,0.));
#12824=DIRECTION('center_axis',(0.,0.,-1.));
#12825=DIRECTION('ref_axis',(1.,0.,0.));
#12826=DIRECTION('',(0.,0.,-1.));
#12827=DIRECTION('center_axis',(0.,0.,-1.));
#12828=DIRECTION('ref_axis',(1.,0.,0.));
#12829=DIRECTION('center_axis',(0.,0.,1.));
#12830=DIRECTION('ref_axis',(1.,0.,0.));
#12831=DIRECTION('center_axis',(0.,0.,1.));
#12832=DIRECTION('ref_axis',(1.,0.,0.));
#12833=DIRECTION('',(0.,0.,-1.));
#12834=DIRECTION('center_axis',(0.,0.,1.));
#12835=DIRECTION('ref_axis',(1.,0.,0.));
#12836=DIRECTION('center_axis',(0.,0.,1.));
#12837=DIRECTION('ref_axis',(1.,0.,0.));
#12838=DIRECTION('center_axis',(0.,0.,1.));
#12839=DIRECTION('ref_axis',(1.,0.,0.));
#16003=CARTESIAN_POINT('',(0.,0.,0.));
#16004=CARTESIAN_POINT('Origin',(10.,2.,9.6));
#16005=CARTESIAN_POINT('',(9.695,2.,10.1));
#16006=CARTESIAN_POINT('Origin',(10.,2.,10.1));
#16007=CARTESIAN_POINT('',(9.695,2.,9.6));
#16008=CARTESIAN_POINT('',(9.695,2.,9.6));
#16009=CARTESIAN_POINT('Origin',(10.,2.,9.6));
#16010=CARTESIAN_POINT('Origin',(10.,2.,9.6));
#16011=CARTESIAN_POINT('',(9.5,2.,10.1));
#16012=CARTESIAN_POINT('Origin',(10.,2.,10.1));
#16013=CARTESIAN_POINT('',(9.5,2.,9.6));
#16014=CARTESIAN_POINT('',(9.5,2.,9.6));
#16015=CARTESIAN_POINT('Origin',(10.,2.,9.6));
#16016=CARTESIAN_POINT('Origin',(10.,2.,10.1));
#16017=CARTESIAN_POINT('Origin',(10.,2.,9.6));
#16600=UNCERTAINTY_MEASURE_WITH_UNIT(LENGTH_MEASURE(0.001),#16679,
'DISTANCE_ACCURACY_VALUE',
'Maximum model space distance between geometric entities at asserted c
onnectivities');
#16614=UNCERTAINTY_MEASURE_WITH_UNIT(LENGTH_MEASURE(0.001),#16679,
'DISTANCE_ACCURACY_VALUE',
'Maximum model space distance between geometric entities at asserted c
onnectivities');
#16664=(
GEOMETRIC_REPRESENTATION_CONTEXT(3)
GLOBAL_UNCERTAINTY_ASSIGNED_CONTEXT((#16600))
GLOBAL_UNIT_ASSIGNED_CONTEXT((#16679,#16681,#16682))
REPRESENTATION_CONTEXT('','3D')
);
#16678=(
GEOMETRIC_REPRESENTATION_CONTEXT(3)
GLOBAL_UNCERTAINTY_ASSIGNED_CONTEXT((#16614))
GLOBAL_UNIT_ASSIGNED_CONTEXT((#16679,#16681,#16682))
REPRESENTATION_CONTEXT('','3D')
);
#16679=(
LENGTH_UNIT()
NAMED_UNIT(*)
SI_UNIT(.CENTI.,.METRE.)
);
#16681=(
NAMED_UNIT(*)
PLANE_ANGLE_UNIT()
SI_UNIT($,.RADIAN.)
);
#16682=(
NAMED_UNIT(*)
SI_UNIT($,.STERADIAN.)
SOLID_ANGLE_UNIT()
);
#16732=SHAPE_DEFINITION_REPRESENTATION(#16806,#16959);
#16806=PRODUCT_DEFINITION_SHAPE('',$,#17023);
#16959=SHAPE_REPRESENTATION('',(#10332),#16664);
#16973=PRODUCT_DEFINITION_CONTEXT('part definition',#17164,'design');
#17023=PRODUCT_DEFINITION('Upper pin sleeve (2)','Upper pin sleeve (2)',#17086,
#16973);
#17086=PRODUCT_DEFINITION_FORMATION('',$,#17215);
#17164=APPLICATION_CONTEXT(
'Core Data for Automotive Mechanical Design Process');
#17165=PRODUCT_CONTEXT('part definition',#17164,'mechanical');
#17215=PRODUCT('Upper pin sleeve (2)','Upper pin sleeve (2)',
'Upper pin sleeve (2)',(#17165));
#17285=COLOUR_RGB('Grey',0.48,0.52,0.57);
#17286=FILL_AREA_STYLE_COLOUR('',#17285);
#17287=FILL_AREA_STYLE('',(#17286));
#17288=SURFACE_STYLE_FILL_AREA(#17287);
#17289=SURFACE_SIDE_STYLE('',(#17288));
#17290=SURFACE_STYLE_USAGE(.BOTH.,#17289);
#17291=PRESENTATION_STYLE_ASSIGNMENT((#17290));
ENDSEC;
END-ISO-10303-21;
